ISO-10303-21;
HEADER;
/* Generated by software containing ST-Developer
 * from STEP Tools, Inc. (www.steptools.com) 
 */

FILE_DESCRIPTION(
/* description */ ('Manual rail carriage with stops'),
/* implementation_level */ '2;1');

FILE_NAME(
/* name */ 'Flat Washer - M5.step',
/* time_stamp */ '2026-10-27T18:54:27-07:00',
/* author */ (''),
/* organization */ (''),
/* preprocessor_version */ 'ST-DEVELOPER v20.2',
/* originating_system */ 'Autodesk Translation Framework v15.17.0.0',
/* authorisation */ '');

FILE_SCHEMA (('AUTOMOTIVE_DESIGN { 1 0 10303 214 3 1 1 }'));
ENDSEC;

DATA;
#10=MECHANICAL_DESIGN_GEOMETRIC_PRESENTATION_REPRESENTATION('',(#287),#8499);
#218=CONICAL_SURFACE('',#5513,0.275,0.785398163397449);
#251=SHAPE_REPRESENTATION_RELATIONSHIP('SRR','None',#8616,#269);
#269=ADVANCED_BREP_SHAPE_REPRESENTATION('',(#303),#8495);
#287=STYLED_ITEM('',(#8795),#303);
#303=MANIFOLD_SOLID_BREP('Body1',#4957);
#374=FACE_BOUND('',#1136,.T.);
#375=FACE_BOUND('',#1139,.T.);
#551=PLANE('',#5518);
#552=PLANE('',#5522);
#799=FACE_OUTER_BOUND('',#1133,.T.);
#800=FACE_OUTER_BOUND('',#1134,.T.);
#801=FACE_OUTER_BOUND('',#1135,.T.);
#802=FACE_OUTER_BOUND('',#1137,.T.);
#803=FACE_OUTER_BOUND('',#1138,.T.);
#1133=EDGE_LOOP('',(#4468,#4469,#4470,#4471));
#1134=EDGE_LOOP('',(#4472,#4473,#4474,#4475));
#1135=EDGE_LOOP('',(#4476));
#1136=EDGE_LOOP('',(#4477));
#1137=EDGE_LOOP('',(#4478,#4479,#4480,#4481));
#1138=EDGE_LOOP('',(#4482));
#1139=EDGE_LOOP('',(#4483));
#1629=LINE('',#8238,#2129);
#1630=LINE('',#8242,#2130);
#1631=LINE('',#8249,#2131);
#2129=VECTOR('',#6784,0.275);
#2130=VECTOR('',#6789,0.265);
#2131=VECTOR('',#6798,0.5);
#2287=CIRCLE('',#5514,0.285);
#2288=CIRCLE('',#5515,0.265);
#2289=CIRCLE('',#5517,0.265);
#2290=CIRCLE('',#5519,0.5);
#2291=CIRCLE('',#5521,0.5);
#2679=VERTEX_POINT('',#8235);
#2680=VERTEX_POINT('',#8237);
#2681=VERTEX_POINT('',#8241);
#2682=VERTEX_POINT('',#8245);
#2683=VERTEX_POINT('',#8248);
#3282=EDGE_CURVE('',#2679,#2679,#2287,.T.);
#3283=EDGE_CURVE('',#2679,#2680,#1629,.T.);
#3284=EDGE_CURVE('',#2680,#2680,#2288,.T.);
#3285=EDGE_CURVE('',#2680,#2681,#1630,.T.);
#3286=EDGE_CURVE('',#2681,#2681,#2289,.T.);
#3287=EDGE_CURVE('',#2682,#2682,#2290,.T.);
#3288=EDGE_CURVE('',#2682,#2683,#1631,.T.);
#3289=EDGE_CURVE('',#2683,#2683,#2291,.T.);
#4468=ORIENTED_EDGE('',*,*,#3282,.T.);
#4469=ORIENTED_EDGE('',*,*,#3283,.T.);
#4470=ORIENTED_EDGE('',*,*,#3284,.T.);
#4471=ORIENTED_EDGE('',*,*,#3283,.F.);
#4472=ORIENTED_EDGE('',*,*,#3284,.F.);
#4473=ORIENTED_EDGE('',*,*,#3285,.T.);
#4474=ORIENTED_EDGE('',*,*,#3286,.T.);
#4475=ORIENTED_EDGE('',*,*,#3285,.F.);
#4476=ORIENTED_EDGE('',*,*,#3287,.T.);
#4477=ORIENTED_EDGE('',*,*,#3282,.F.);
#4478=ORIENTED_EDGE('',*,*,#3287,.F.);
#4479=ORIENTED_EDGE('',*,*,#3288,.T.);
#4480=ORIENTED_EDGE('',*,*,#3289,.T.);
#4481=ORIENTED_EDGE('',*,*,#3288,.F.);
#4482=ORIENTED_EDGE('',*,*,#3289,.F.);
#4483=ORIENTED_EDGE('',*,*,#3286,.F.);
#4668=CYLINDRICAL_SURFACE('',#5516,0.265);
#4669=CYLINDRICAL_SURFACE('',#5520,0.5);
#4898=ADVANCED_FACE('',(#799),#218,.F.);
#4899=ADVANCED_FACE('',(#800),#4668,.F.);
#4900=ADVANCED_FACE('',(#801,#374),#551,.T.);
#4901=ADVANCED_FACE('',(#802),#4669,.T.);
#4902=ADVANCED_FACE('',(#803,#375),#552,.F.);
#4957=CLOSED_SHELL('',(#4898,#4899,#4900,#4901,#4902));
#5512=AXIS2_PLACEMENT_3D('',#8233,#6778,#6779);
#5513=AXIS2_PLACEMENT_3D('',#8234,#6780,#6781);
#5514=AXIS2_PLACEMENT_3D('',#8236,#6782,#6783);
#5515=AXIS2_PLACEMENT_3D('',#8239,#6785,#6786);
#5516=AXIS2_PLACEMENT_3D('',#8240,#6787,#6788);
#5517=AXIS2_PLACEMENT_3D('',#8243,#6790,#6791);
#5518=AXIS2_PLACEMENT_3D('',#8244,#6792,#6793);
#5519=AXIS2_PLACEMENT_3D('',#8246,#6794,#6795);
#5520=AXIS2_PLACEMENT_3D('',#8247,#6796,#6797);
#5521=AXIS2_PLACEMENT_3D('',#8250,#6799,#6800);
#5522=AXIS2_PLACEMENT_3D('',#8251,#6801,#6802);
#6778=DIRECTION('axis',(0.,0.,1.));
#6779=DIRECTION('refdir',(1.,0.,0.));
#6780=DIRECTION('center_axis',(0.,1.,0.));
#6781=DIRECTION('ref_axis',(1.,0.,0.));
#6782=DIRECTION('center_axis',(0.,1.,0.));
#6783=DIRECTION('ref_axis',(1.,0.,0.));
#6784=DIRECTION('',(0.707106781186548,-0.707106781186547,-8.65956056235494E-17));
#6785=DIRECTION('center_axis',(0.,-1.,0.));
#6786=DIRECTION('ref_axis',(1.,0.,0.));
#6787=DIRECTION('center_axis',(0.,1.,0.));
#6788=DIRECTION('ref_axis',(1.,0.,0.));
#6789=DIRECTION('',(0.,-1.,0.));
#6790=DIRECTION('center_axis',(0.,-1.,0.));
#6791=DIRECTION('ref_axis',(1.,0.,0.));
#6792=DIRECTION('center_axis',(0.,1.,0.));
#6793=DIRECTION('ref_axis',(1.,0.,0.));
#6794=DIRECTION('center_axis',(0.,1.,0.));
#6795=DIRECTION('ref_axis',(1.,0.,0.));
#6796=DIRECTION('center_axis',(0.,1.,0.));
#6797=DIRECTION('ref_axis',(1.,0.,0.));
#6798=DIRECTION('',(0.,-1.,0.));
#6799=DIRECTION('center_axis',(0.,1.,0.));
#6800=DIRECTION('ref_axis',(1.,0.,0.));
#6801=DIRECTION('center_axis',(0.,1.,0.));
#6802=DIRECTION('ref_axis',(1.,0.,0.));
#8233=CARTESIAN_POINT('',(0.,0.,0.));
#8234=CARTESIAN_POINT('Origin',(0.,0.09,0.));
#8235=CARTESIAN_POINT('',(-0.285,0.1,3.49024337756996E-17));
#8236=CARTESIAN_POINT('Origin',(0.,0.1,0.));
#8237=CARTESIAN_POINT('',(-0.265,0.08,-3.24531401774049E-17));
#8238=CARTESIAN_POINT('',(-0.275,0.09,3.36777869765522E-17));
#8239=CARTESIAN_POINT('Origin',(0.,0.08,0.));
#8240=CARTESIAN_POINT('Origin',(0.,0.,0.));
#8241=CARTESIAN_POINT('',(-0.265,0.,3.24531401774049E-17));
#8242=CARTESIAN_POINT('',(-0.265,0.,3.24531401774049E-17));
#8243=CARTESIAN_POINT('Origin',(0.,0.,0.));
#8244=CARTESIAN_POINT('Origin',(0.,0.1,0.));
#8245=CARTESIAN_POINT('',(-0.5,0.1,6.12323399573677E-17));
#8246=CARTESIAN_POINT('Origin',(0.,0.1,0.));
#8247=CARTESIAN_POINT('Origin',(0.,0.,0.));
#8248=CARTESIAN_POINT('',(-0.5,0.,6.12323399573677E-17));
#8249=CARTESIAN_POINT('',(-0.5,0.,6.12323399573677E-17));
#8250=CARTESIAN_POINT('Origin',(0.,0.,0.));
#8251=CARTESIAN_POINT('Origin',(0.,0.,0.));
#8472=UNCERTAINTY_MEASURE_WITH_UNIT(LENGTH_MEASURE(0.001),#8500,
'DISTANCE_ACCURACY_VALUE',
'Maximum model space distance between geometric entities at asserted c
onnectivities');
#8476=UNCERTAINTY_MEASURE_WITH_UNIT(LENGTH_MEASURE(0.001),#8500,
'DISTANCE_ACCURACY_VALUE',
'Maximum model space distance between geometric entities at asserted c
onnectivities');
#8495=(
GEOMETRIC_REPRESENTATION_CONTEXT(3)
GLOBAL_UNCERTAINTY_ASSIGNED_CONTEXT((#8472))
GLOBAL_UNIT_ASSIGNED_CONTEXT((#8500,#8502,#8503))
REPRESENTATION_CONTEXT('','3D')
);
#8499=(
GEOMETRIC_REPRESENTATION_CONTEXT(3)
GLOBAL_UNCERTAINTY_ASSIGNED_CONTEXT((#8476))
GLOBAL_UNIT_ASSIGNED_CONTEXT((#8500,#8502,#8503))
REPRESENTATION_CONTEXT('','3D')
);
#8500=(
LENGTH_UNIT()
NAMED_UNIT(*)
SI_UNIT(.CENTI.,.METRE.)
);
#8502=(
NAMED_UNIT(*)
PLANE_ANGLE_UNIT()
SI_UNIT($,.RADIAN.)
);
#8503=(
NAMED_UNIT(*)
SI_UNIT($,.STERADIAN.)
SOLID_ANGLE_UNIT()
);
#8522=SHAPE_DEFINITION_REPRESENTATION(#8547,#8616);
#8547=PRODUCT_DEFINITION_SHAPE('',$,#8639);
#8616=SHAPE_REPRESENTATION('',(#5512),#8495);
#8620=PRODUCT_DEFINITION_CONTEXT('part definition',#8688,'design');
#8639=PRODUCT_DEFINITION('Flat Washer - M5','Flat Washer - M5',#8661,#8620);
#8661=PRODUCT_DEFINITION_FORMATION('',$,#8708);
#8688=APPLICATION_CONTEXT(
'Core Data for Automotive Mechanical Design Process');
#8689=PRODUCT_CONTEXT('part definition',#8688,'mechanical');
#8708=PRODUCT('Flat Washer - M5','Flat Washer - M5','Flat Washer - M5',
(#8689));
#8789=COLOUR_RGB('Black',0.12,0.14,0.17);
#8790=FILL_AREA_STYLE_COLOUR('',#8789);
#8791=FILL_AREA_STYLE('',(#8790));
#8792=SURFACE_STYLE_FILL_AREA(#8791);
#8793=SURFACE_SIDE_STYLE('',(#8792));
#8794=SURFACE_STYLE_USAGE(.BOTH.,#8793);
#8795=PRESENTATION_STYLE_ASSIGNMENT((#8794));
ENDSEC;
END-ISO-10303-21;
